ISO-10303-21;
HEADER;
/* Generated by software containing ST-Developer
 * from STEP Tools, Inc. (www.steptools.com) 
 */

FILE_DESCRIPTION(
/* description */ ('Bell-crank linkage with push rods'),
/* implementation_level */ '2;1');

FILE_NAME(
/* name */ 'Horizontal guide cap (1).step',
/* time_stamp */ '2026-10-28T03:25:15-07:00',
/* author */ (''),
/* organization */ (''),
/* preprocessor_version */ 'ST-DEVELOPER v20.2',
/* originating_system */ 'Autodesk Translation Framework v15.17.0.0',
/* authorisation */ '');

FILE_SCHEMA (('AUTOMOTIVE_DESIGN { 1 0 10303 214 3 1 1 }'));
ENDSEC;

DATA;
#10=MECHANICAL_DESIGN_GEOMETRIC_PRESENTATION_REPRESENTATION('',(#651),#16678);
#535=SHAPE_REPRESENTATION_RELATIONSHIP('SRR','None',#16956,#589);
#589=ADVANCED_BREP_SHAPE_REPRESENTATION('',(#711),#16661);
#651=STYLED_ITEM('',(#17284),#711);
#711=MANIFOLD_SOLID_BREP('Body1',#8843);
#895=FACE_BOUND('',#2339,.T.);
#896=FACE_BOUND('',#2340,.T.);
#897=FACE_BOUND('',#2341,.T.);
#898=FACE_BOUND('',#2342,.T.);
#899=FACE_BOUND('',#2343,.T.);
#900=FACE_BOUND('',#2346,.T.);
#901=FACE_BOUND('',#2347,.T.);
#902=FACE_BOUND('',#2348,.T.);
#903=FACE_BOUND('',#2349,.T.);
#904=FACE_BOUND('',#2350,.T.);
#1172=PLANE('',#10299);
#1173=PLANE('',#10300);
#1174=PLANE('',#10301);
#1175=PLANE('',#10302);
#1176=PLANE('',#10303);
#1177=PLANE('',#10304);
#1640=FACE_OUTER_BOUND('',#2332,.T.);
#1641=FACE_OUTER_BOUND('',#2333,.T.);
#1642=FACE_OUTER_BOUND('',#2334,.T.);
#1643=FACE_OUTER_BOUND('',#2335,.T.);
#1644=FACE_OUTER_BOUND('',#2336,.T.);
#1645=FACE_OUTER_BOUND('',#2337,.T.);
#1646=FACE_OUTER_BOUND('',#2338,.T.);
#1647=FACE_OUTER_BOUND('',#2344,.T.);
#1648=FACE_OUTER_BOUND('',#2345,.T.);
#1649=FACE_OUTER_BOUND('',#2351,.T.);
#1650=FACE_OUTER_BOUND('',#2352,.T.);
#2332=EDGE_LOOP('',(#7569,#7570,#7571,#7572));
#2333=EDGE_LOOP('',(#7573,#7574,#7575,#7576));
#2334=EDGE_LOOP('',(#7577,#7578,#7579,#7580));
#2335=EDGE_LOOP('',(#7581,#7582,#7583,#7584));
#2336=EDGE_LOOP('',(#7585,#7586,#7587,#7588));
#2337=EDGE_LOOP('',(#7589,#7590,#7591,#7592));
#2338=EDGE_LOOP('',(#7593,#7594,#7595,#7596));
#2339=EDGE_LOOP('',(#7597));
#2340=EDGE_LOOP('',(#7598));
#2341=EDGE_LOOP('',(#7599));
#2342=EDGE_LOOP('',(#7600));
#2343=EDGE_LOOP('',(#7601));
#2344=EDGE_LOOP('',(#7602,#7603,#7604,#7605));
#2345=EDGE_LOOP('',(#7606,#7607,#7608,#7609));
#2346=EDGE_LOOP('',(#7610));
#2347=EDGE_LOOP('',(#7611));
#2348=EDGE_LOOP('',(#7612));
#2349=EDGE_LOOP('',(#7613));
#2350=EDGE_LOOP('',(#7614));
#2351=EDGE_LOOP('',(#7615,#7616,#7617,#7618));
#2352=EDGE_LOOP('',(#7619,#7620,#7621,#7622));
#2943=LINE('',#15906,#3492);
#2944=LINE('',#15912,#3493);
#2945=LINE('',#15918,#3494);
#2946=LINE('',#15924,#3495);
#2947=LINE('',#15930,#3496);
#2948=LINE('',#15935,#3497);
#2949=LINE('',#15937,#3498);
#2950=LINE('',#15939,#3499);
#2951=LINE('',#15940,#3500);
#2952=LINE('',#15943,#3501);
#2953=LINE('',#15945,#3502);
#2954=LINE('',#15946,#3503);
#2955=LINE('',#15949,#3504);
#2956=LINE('',#15951,#3505);
#2957=LINE('',#15952,#3506);
#2958=LINE('',#15954,#3507);
#2959=LINE('',#15955,#3508);
#3492=VECTOR('',#12705,0.225);
#3493=VECTOR('',#12712,0.225);
#3494=VECTOR('',#12719,0.225);
#3495=VECTOR('',#12726,0.225);
#3496=VECTOR('',#12733,0.7);
#3497=VECTOR('',#12738,1.);
#3498=VECTOR('',#12739,1.);
#3499=VECTOR('',#12740,1.);
#3500=VECTOR('',#12741,1.);
#3501=VECTOR('',#12744,1.);
#3502=VECTOR('',#12745,1.);
#3503=VECTOR('',#12746,1.);
#3504=VECTOR('',#12749,1.);
#3505=VECTOR('',#12750,1.);
#3506=VECTOR('',#12751,1.);
#3507=VECTOR('',#12754,1.);
#3508=VECTOR('',#12755,1.);
#4009=CIRCLE('',#10285,0.225);
#4010=CIRCLE('',#10286,0.225);
#4011=CIRCLE('',#10288,0.225);
#4012=CIRCLE('',#10289,0.225);
#4013=CIRCLE('',#10291,0.225);
#4014=CIRCLE('',#10292,0.225);
#4015=CIRCLE('',#10294,0.225);
#4016=CIRCLE('',#10295,0.225);
#4017=CIRCLE('',#10297,0.7);
#4018=CIRCLE('',#10298,0.7);
#4668=VERTEX_POINT('',#15903);
#4669=VERTEX_POINT('',#15905);
#4670=VERTEX_POINT('',#15909);
#4671=VERTEX_POINT('',#15911);
#4672=VERTEX_POINT('',#15915);
#4673=VERTEX_POINT('',#15917);
#4674=VERTEX_POINT('',#15921);
#4675=VERTEX_POINT('',#15923);
#4676=VERTEX_POINT('',#15927);
#4677=VERTEX_POINT('',#15929);
#4678=VERTEX_POINT('',#15933);
#4679=VERTEX_POINT('',#15934);
#4680=VERTEX_POINT('',#15936);
#4681=VERTEX_POINT('',#15938);
#4682=VERTEX_POINT('',#15942);
#4683=VERTEX_POINT('',#15944);
#4684=VERTEX_POINT('',#15948);
#4685=VERTEX_POINT('',#15950);
#5662=EDGE_CURVE('',#4668,#4668,#4009,.T.);
#5663=EDGE_CURVE('',#4668,#4669,#2943,.T.);
#5664=EDGE_CURVE('',#4669,#4669,#4010,.T.);
#5665=EDGE_CURVE('',#4670,#4670,#4011,.T.);
#5666=EDGE_CURVE('',#4670,#4671,#2944,.T.);
#5667=EDGE_CURVE('',#4671,#4671,#4012,.T.);
#5668=EDGE_CURVE('',#4672,#4672,#4013,.T.);
#5669=EDGE_CURVE('',#4672,#4673,#2945,.T.);
#5670=EDGE_CURVE('',#4673,#4673,#4014,.T.);
#5671=EDGE_CURVE('',#4674,#4674,#4015,.T.);
#5672=EDGE_CURVE('',#4674,#4675,#2946,.T.);
#5673=EDGE_CURVE('',#4675,#4675,#4016,.T.);
#5674=EDGE_CURVE('',#4676,#4676,#4017,.T.);
#5675=EDGE_CURVE('',#4676,#4677,#2947,.T.);
#5676=EDGE_CURVE('',#4677,#4677,#4018,.T.);
#5677=EDGE_CURVE('',#4678,#4679,#2948,.T.);
#5678=EDGE_CURVE('',#4679,#4680,#2949,.T.);
#5679=EDGE_CURVE('',#4681,#4680,#2950,.T.);
#5680=EDGE_CURVE('',#4678,#4681,#2951,.T.);
#5681=EDGE_CURVE('',#4682,#4678,#2952,.T.);
#5682=EDGE_CURVE('',#4683,#4681,#2953,.T.);
#5683=EDGE_CURVE('',#4682,#4683,#2954,.T.);
#5684=EDGE_CURVE('',#4684,#4682,#2955,.T.);
#5685=EDGE_CURVE('',#4685,#4683,#2956,.T.);
#5686=EDGE_CURVE('',#4684,#4685,#2957,.T.);
#5687=EDGE_CURVE('',#4679,#4684,#2958,.T.);
#5688=EDGE_CURVE('',#4680,#4685,#2959,.T.);
#7569=ORIENTED_EDGE('',*,*,#5662,.F.);
#7570=ORIENTED_EDGE('',*,*,#5663,.T.);
#7571=ORIENTED_EDGE('',*,*,#5664,.F.);
#7572=ORIENTED_EDGE('',*,*,#5663,.F.);
#7573=ORIENTED_EDGE('',*,*,#5665,.F.);
#7574=ORIENTED_EDGE('',*,*,#5666,.T.);
#7575=ORIENTED_EDGE('',*,*,#5667,.F.);
#7576=ORIENTED_EDGE('',*,*,#5666,.F.);
#7577=ORIENTED_EDGE('',*,*,#5668,.F.);
#7578=ORIENTED_EDGE('',*,*,#5669,.T.);
#7579=ORIENTED_EDGE('',*,*,#5670,.F.);
#7580=ORIENTED_EDGE('',*,*,#5669,.F.);
#7581=ORIENTED_EDGE('',*,*,#5671,.F.);
#7582=ORIENTED_EDGE('',*,*,#5672,.T.);
#7583=ORIENTED_EDGE('',*,*,#5673,.F.);
#7584=ORIENTED_EDGE('',*,*,#5672,.F.);
#7585=ORIENTED_EDGE('',*,*,#5674,.F.);
#7586=ORIENTED_EDGE('',*,*,#5675,.T.);
#7587=ORIENTED_EDGE('',*,*,#5676,.F.);
#7588=ORIENTED_EDGE('',*,*,#5675,.F.);
#7589=ORIENTED_EDGE('',*,*,#5677,.T.);
#7590=ORIENTED_EDGE('',*,*,#5678,.T.);
#7591=ORIENTED_EDGE('',*,*,#5679,.F.);
#7592=ORIENTED_EDGE('',*,*,#5680,.F.);
#7593=ORIENTED_EDGE('',*,*,#5681,.T.);
#7594=ORIENTED_EDGE('',*,*,#5680,.T.);
#7595=ORIENTED_EDGE('',*,*,#5682,.F.);
#7596=ORIENTED_EDGE('',*,*,#5683,.F.);
#7597=ORIENTED_EDGE('',*,*,#5676,.T.);
#7598=ORIENTED_EDGE('',*,*,#5673,.T.);
#7599=ORIENTED_EDGE('',*,*,#5670,.T.);
#7600=ORIENTED_EDGE('',*,*,#5667,.T.);
#7601=ORIENTED_EDGE('',*,*,#5664,.T.);
#7602=ORIENTED_EDGE('',*,*,#5684,.T.);
#7603=ORIENTED_EDGE('',*,*,#5683,.T.);
#7604=ORIENTED_EDGE('',*,*,#5685,.F.);
#7605=ORIENTED_EDGE('',*,*,#5686,.F.);
#7606=ORIENTED_EDGE('',*,*,#5687,.T.);
#7607=ORIENTED_EDGE('',*,*,#5686,.T.);
#7608=ORIENTED_EDGE('',*,*,#5688,.F.);
#7609=ORIENTED_EDGE('',*,*,#5678,.F.);
#7610=ORIENTED_EDGE('',*,*,#5674,.T.);
#7611=ORIENTED_EDGE('',*,*,#5671,.T.);
#7612=ORIENTED_EDGE('',*,*,#5668,.T.);
#7613=ORIENTED_EDGE('',*,*,#5665,.T.);
#7614=ORIENTED_EDGE('',*,*,#5662,.T.);
#7615=ORIENTED_EDGE('',*,*,#5688,.T.);
#7616=ORIENTED_EDGE('',*,*,#5685,.T.);
#7617=ORIENTED_EDGE('',*,*,#5682,.T.);
#7618=ORIENTED_EDGE('',*,*,#5679,.T.);
#7619=ORIENTED_EDGE('',*,*,#5687,.F.);
#7620=ORIENTED_EDGE('',*,*,#5677,.F.);
#7621=ORIENTED_EDGE('',*,*,#5681,.F.);
#7622=ORIENTED_EDGE('',*,*,#5684,.F.);
#8221=CYLINDRICAL_SURFACE('',#10284,0.225);
#8222=CYLINDRICAL_SURFACE('',#10287,0.225);
#8223=CYLINDRICAL_SURFACE('',#10290,0.225);
#8224=CYLINDRICAL_SURFACE('',#10293,0.225);
#8225=CYLINDRICAL_SURFACE('',#10296,0.7);
#8665=ADVANCED_FACE('',(#1640),#8221,.F.);
#8666=ADVANCED_FACE('',(#1641),#8222,.F.);
#8667=ADVANCED_FACE('',(#1642),#8223,.F.);
#8668=ADVANCED_FACE('',(#1643),#8224,.F.);
#8669=ADVANCED_FACE('',(#1644),#8225,.F.);
#8670=ADVANCED_FACE('',(#1645),#1172,.T.);
#8671=ADVANCED_FACE('',(#1646,#895,#896,#897,#898,#899),#1173,.T.);
#8672=ADVANCED_FACE('',(#1647),#1174,.T.);
#8673=ADVANCED_FACE('',(#1648,#900,#901,#902,#903,#904),#1175,.T.);
#8674=ADVANCED_FACE('',(#1649),#1176,.T.);
#8675=ADVANCED_FACE('',(#1650),#1177,.F.);
#8843=CLOSED_SHELL('',(#8665,#8666,#8667,#8668,#8669,#8670,#8671,#8672,
#8673,#8674,#8675));
#10283=AXIS2_PLACEMENT_3D('',#15901,#12699,#12700);
#10284=AXIS2_PLACEMENT_3D('',#15902,#12701,#12702);
#10285=AXIS2_PLACEMENT_3D('',#15904,#12703,#12704);
#10286=AXIS2_PLACEMENT_3D('',#15907,#12706,#12707);
#10287=AXIS2_PLACEMENT_3D('',#15908,#12708,#12709);
#10288=AXIS2_PLACEMENT_3D('',#15910,#12710,#12711);
#10289=AXIS2_PLACEMENT_3D('',#15913,#12713,#12714);
#10290=AXIS2_PLACEMENT_3D('',#15914,#12715,#12716);
#10291=AXIS2_PLACEMENT_3D('',#15916,#12717,#12718);
#10292=AXIS2_PLACEMENT_3D('',#15919,#12720,#12721);
#10293=AXIS2_PLACEMENT_3D('',#15920,#12722,#12723);
#10294=AXIS2_PLACEMENT_3D('',#15922,#12724,#12725);
#10295=AXIS2_PLACEMENT_3D('',#15925,#12727,#12728);
#10296=AXIS2_PLACEMENT_3D('',#15926,#12729,#12730);
#10297=AXIS2_PLACEMENT_3D('',#15928,#12731,#12732);
#10298=AXIS2_PLACEMENT_3D('',#15931,#12734,#12735);
#10299=AXIS2_PLACEMENT_3D('',#15932,#12736,#12737);
#10300=AXIS2_PLACEMENT_3D('',#15941,#12742,#12743);
#10301=AXIS2_PLACEMENT_3D('',#15947,#12747,#12748);
#10302=AXIS2_PLACEMENT_3D('',#15953,#12752,#12753);
#10303=AXIS2_PLACEMENT_3D('',#15956,#12756,#12757);
#10304=AXIS2_PLACEMENT_3D('',#15957,#12758,#12759);
#12699=DIRECTION('axis',(0.,0.,1.));
#12700=DIRECTION('refdir',(1.,0.,0.));
#12701=DIRECTION('center_axis',(1.,0.,0.));
#12702=DIRECTION('ref_axis',(0.,0.,-1.));
#12703=DIRECTION('center_axis',(1.,0.,0.));
#12704=DIRECTION('ref_axis',(0.,0.,-1.));
#12705=DIRECTION('',(1.,0.,0.));
#12706=DIRECTION('center_axis',(-1.,0.,0.));
#12707=DIRECTION('ref_axis',(0.,0.,-1.));
#12708=DIRECTION('center_axis',(1.,0.,0.));
#12709=DIRECTION('ref_axis',(0.,0.,-1.));
#12710=DIRECTION('center_axis',(1.,0.,0.));
#12711=DIRECTION('ref_axis',(0.,0.,-1.));
#12712=DIRECTION('',(1.,0.,0.));
#12713=DIRECTION('center_axis',(-1.,0.,0.));
#12714=DIRECTION('ref_axis',(0.,0.,-1.));
#12715=DIRECTION('center_axis',(1.,0.,0.));
#12716=DIRECTION('ref_axis',(0.,0.,-1.));
#12717=DIRECTION('center_axis',(1.,0.,0.));
#12718=DIRECTION('ref_axis',(0.,0.,-1.));
#12719=DIRECTION('',(1.,0.,0.));
#12720=DIRECTION('center_axis',(-1.,0.,0.));
#12721=DIRECTION('ref_axis',(0.,0.,-1.));
#12722=DIRECTION('center_axis',(1.,0.,0.));
#12723=DIRECTION('ref_axis',(0.,0.,-1.));
#12724=DIRECTION('center_axis',(1.,0.,0.));
#12725=DIRECTION('ref_axis',(0.,0.,-1.));
#12726=DIRECTION('',(1.,0.,0.));
#12727=DIRECTION('center_axis',(-1.,0.,0.));
#12728=DIRECTION('ref_axis',(0.,0.,-1.));
#12729=DIRECTION('center_axis',(1.,0.,0.));
#12730=DIRECTION('ref_axis',(0.,0.,-1.));
#12731=DIRECTION('center_axis',(1.,0.,0.));
#12732=DIRECTION('ref_axis',(0.,0.,-1.));
#12733=DIRECTION('',(1.,0.,0.));
#12734=DIRECTION('center_axis',(-1.,0.,0.));
#12735=DIRECTION('ref_axis',(0.,0.,-1.));
#12736=DIRECTION('center_axis',(0.,1.,0.));
#12737=DIRECTION('ref_axis',(-1.,0.,0.));
#12738=DIRECTION('',(-1.,0.,0.));
#12739=DIRECTION('',(0.,0.,1.));
#12740=DIRECTION('',(-1.,0.,0.));
#12741=DIRECTION('',(0.,0.,1.));
#12742=DIRECTION('center_axis',(1.,0.,0.));
#12743=DIRECTION('ref_axis',(0.,1.,0.));
#12744=DIRECTION('',(0.,1.,0.));
#12745=DIRECTION('',(0.,1.,0.));
#12746=DIRECTION('',(0.,0.,1.));
#12747=DIRECTION('center_axis',(0.,-1.,0.));
#12748=DIRECTION('ref_axis',(1.,0.,0.));
#12749=DIRECTION('',(1.,0.,0.));
#12750=DIRECTION('',(1.,0.,0.));
#12751=DIRECTION('',(0.,0.,1.));
#12752=DIRECTION('center_axis',(-1.,0.,0.));
#12753=DIRECTION('ref_axis',(0.,-1.,0.));
#12754=DIRECTION('',(0.,-1.,0.));
#12755=DIRECTION('',(0.,-1.,0.));
#12756=DIRECTION('center_axis',(0.,0.,1.));
#12757=DIRECTION('ref_axis',(1.,0.,0.));
#12758=DIRECTION('center_axis',(0.,0.,1.));
#12759=DIRECTION('ref_axis',(1.,0.,0.));
#15901=CARTESIAN_POINT('',(0.,0.,0.));
#15902=CARTESIAN_POINT('Origin',(11.4,3.2,2.8));
#15903=CARTESIAN_POINT('',(11.5,3.2,3.025));
#15904=CARTESIAN_POINT('Origin',(11.5,3.2,2.8));
#15905=CARTESIAN_POINT('',(11.8,3.2,3.025));
#15906=CARTESIAN_POINT('',(11.4,3.2,3.025));
#15907=CARTESIAN_POINT('Origin',(11.8,3.2,2.8));
#15908=CARTESIAN_POINT('Origin',(11.4,0.8,5.2));
#15909=CARTESIAN_POINT('',(11.5,0.8,5.425));
#15910=CARTESIAN_POINT('Origin',(11.5,0.8,5.2));
#15911=CARTESIAN_POINT('',(11.8,0.8,5.425));
#15912=CARTESIAN_POINT('',(11.4,0.8,5.425));
#15913=CARTESIAN_POINT('Origin',(11.8,0.8,5.2));
#15914=CARTESIAN_POINT('Origin',(11.4,0.8,2.8));
#15915=CARTESIAN_POINT('',(11.5,0.8,3.025));
#15916=CARTESIAN_POINT('Origin',(11.5,0.8,2.8));
#15917=CARTESIAN_POINT('',(11.8,0.8,3.025));
#15918=CARTESIAN_POINT('',(11.4,0.8,3.025));
#15919=CARTESIAN_POINT('Origin',(11.8,0.8,2.8));
#15920=CARTESIAN_POINT('Origin',(11.4,3.2,5.2));
#15921=CARTESIAN_POINT('',(11.5,3.2,5.425));
#15922=CARTESIAN_POINT('Origin',(11.5,3.2,5.2));
#15923=CARTESIAN_POINT('',(11.8,3.2,5.425));
#15924=CARTESIAN_POINT('',(11.4,3.2,5.425));
#15925=CARTESIAN_POINT('Origin',(11.8,3.2,5.2));
#15926=CARTESIAN_POINT('Origin',(11.4,2.,4.));
#15927=CARTESIAN_POINT('',(11.5,2.,4.7));
#15928=CARTESIAN_POINT('Origin',(11.5,2.,4.));
#15929=CARTESIAN_POINT('',(11.8,2.,4.7));
#15930=CARTESIAN_POINT('',(11.4,2.,4.7));
#15931=CARTESIAN_POINT('Origin',(11.8,2.,4.));
#15932=CARTESIAN_POINT('Origin',(11.8,3.7,2.3));
#15933=CARTESIAN_POINT('',(11.8,3.7,2.3));
#15934=CARTESIAN_POINT('',(11.5,3.7,2.3));
#15935=CARTESIAN_POINT('',(11.8,3.7,2.3));
#15936=CARTESIAN_POINT('',(11.5,3.7,5.7));
#15937=CARTESIAN_POINT('',(11.5,3.7,2.3));
#15938=CARTESIAN_POINT('',(11.8,3.7,5.7));
#15939=CARTESIAN_POINT('',(11.8,3.7,5.7));
#15940=CARTESIAN_POINT('',(11.8,3.7,2.3));
#15941=CARTESIAN_POINT('Origin',(11.8,0.3,2.3));
#15942=CARTESIAN_POINT('',(11.8,0.3,2.3));
#15943=CARTESIAN_POINT('',(11.8,0.3,2.3));
#15944=CARTESIAN_POINT('',(11.8,0.3,5.7));
#15945=CARTESIAN_POINT('',(11.8,0.3,5.7));
#15946=CARTESIAN_POINT('',(11.8,0.3,2.3));
#15947=CARTESIAN_POINT('Origin',(11.5,0.3,2.3));
#15948=CARTESIAN_POINT('',(11.5,0.3,2.3));
#15949=CARTESIAN_POINT('',(11.5,0.3,2.3));
#15950=CARTESIAN_POINT('',(11.5,0.3,5.7));
#15951=CARTESIAN_POINT('',(11.5,0.3,5.7));
#15952=CARTESIAN_POINT('',(11.5,0.3,2.3));
#15953=CARTESIAN_POINT('Origin',(11.5,3.7,2.3));
#15954=CARTESIAN_POINT('',(11.5,3.7,2.3));
#15955=CARTESIAN_POINT('',(11.5,3.7,5.7));
#15956=CARTESIAN_POINT('Origin',(11.65,2.,5.7));
#15957=CARTESIAN_POINT('Origin',(11.65,2.,2.3));
#16597=UNCERTAINTY_MEASURE_WITH_UNIT(LENGTH_MEASURE(0.001),#16679,
'DISTANCE_ACCURACY_VALUE',
'Maximum model space distance between geometric entities at asserted c
onnectivities');
#16614=UNCERTAINTY_MEASURE_WITH_UNIT(LENGTH_MEASURE(0.001),#16679,
'DISTANCE_ACCURACY_VALUE',
'Maximum model space distance between geometric entities at asserted c
onnectivities');
#16661=(
GEOMETRIC_REPRESENTATION_CONTEXT(3)
GLOBAL_UNCERTAINTY_ASSIGNED_CONTEXT((#16597))
GLOBAL_UNIT_ASSIGNED_CONTEXT((#16679,#16681,#16682))
REPRESENTATION_CONTEXT('','3D')
);
#16678=(
GEOMETRIC_REPRESENTATION_CONTEXT(3)
GLOBAL_UNCERTAINTY_ASSIGNED_CONTEXT((#16614))
GLOBAL_UNIT_ASSIGNED_CONTEXT((#16679,#16681,#16682))
REPRESENTATION_CONTEXT('','3D')
);
#16679=(
LENGTH_UNIT()
NAMED_UNIT(*)
SI_UNIT(.CENTI.,.METRE.)
);
#16681=(
NAMED_UNIT(*)
PLANE_ANGLE_UNIT()
SI_UNIT($,.RADIAN.)
);
#16682=(
NAMED_UNIT(*)
SI_UNIT($,.STERADIAN.)
SOLID_ANGLE_UNIT()
);
#16729=SHAPE_DEFINITION_REPRESENTATION(#16803,#16956);
#16803=PRODUCT_DEFINITION_SHAPE('',$,#17020);
#16956=SHAPE_REPRESENTATION('',(#10283),#16661);
#16973=PRODUCT_DEFINITION_CONTEXT('part definition',#17164,'design');
#17020=PRODUCT_DEFINITION('Horizontal guide cap (1)',
'Horizontal guide cap (1)',#17083,#16973);
#17083=PRODUCT_DEFINITION_FORMATION('',$,#17212);
#17164=APPLICATION_CONTEXT(
'Core Data for Automotive Mechanical Design Process');
#17165=PRODUCT_CONTEXT('part definition',#17164,'mechanical');
#17212=PRODUCT('Horizontal guide cap (1)','Horizontal guide cap (1)',
'Horizontal guide cap (1)',(#17165));
#17278=COLOUR_RGB('Sky Blue',0.24,0.69,0.87);
#17279=FILL_AREA_STYLE_COLOUR('',#17278);
#17280=FILL_AREA_STYLE('',(#17279));
#17281=SURFACE_STYLE_FILL_AREA(#17280);
#17282=SURFACE_SIDE_STYLE('',(#17281));
#17283=SURFACE_STYLE_USAGE(.BOTH.,#17282);
#17284=PRESENTATION_STYLE_ASSIGNMENT((#17283));
ENDSEC;
END-ISO-10303-21;
